ISO-10303-21;
HEADER;
/* Generated by software containing ST-Developer
 * from STEP Tools, Inc. (www.steptools.com) 
 */

FILE_DESCRIPTION(
/* description */ ('Compact intermittent indexer'),
/* implementation_level */ '2;1');

FILE_NAME(
/* name */ 'Bearing cap (1).step',
/* time_stamp */ '2026-10-29T16:32:17-07:00',
/* author */ (''),
/* organization */ (''),
/* preprocessor_version */ 'ST-DEVELOPER v20.2',
/* originating_system */ 'Autodesk Translation Framework v15.17.0.0',
/* authorisation */ '');

FILE_SCHEMA (('AUTOMOTIVE_DESIGN { 1 0 10303 214 3 1 1 }'));
ENDSEC;

DATA;
#10=MECHANICAL_DESIGN_GEOMETRIC_PRESENTATION_REPRESENTATION('',(#261),#10837);
#213=SHAPE_REPRESENTATION_RELATIONSHIP('SRR','None',#10947,#237);
#237=ADVANCED_BREP_SHAPE_REPRESENTATION('',(#293),#10814);
#261=STYLED_ITEM('',(#11166),#293);
#293=MANIFOLD_SOLID_BREP('Body1',#5633);
#411=FACE_BOUND('',#1131,.T.);
#412=FACE_BOUND('',#1133,.T.);
#413=FACE_BOUND('',#1136,.T.);
#414=FACE_BOUND('',#1139,.T.);
#415=FACE_BOUND('',#1142,.T.);
#416=FACE_BOUND('',#1149,.T.);
#417=FACE_BOUND('',#1153,.T.);
#418=FACE_BOUND('',#1154,.T.);
#419=FACE_BOUND('',#1155,.T.);
#420=FACE_BOUND('',#1156,.T.);
#421=FACE_BOUND('',#1157,.T.);
#521=PLANE('',#6117);
#522=PLANE('',#6121);
#523=PLANE('',#6127);
#524=PLANE('',#6133);
#525=PLANE('',#6139);
#526=PLANE('',#6156);
#527=PLANE('',#6161);
#743=FACE_OUTER_BOUND('',#1129,.T.);
#744=FACE_OUTER_BOUND('',#1130,.T.);
#745=FACE_OUTER_BOUND('',#1132,.T.);
#746=FACE_OUTER_BOUND('',#1134,.T.);
#747=FACE_OUTER_BOUND('',#1135,.T.);
#748=FACE_OUTER_BOUND('',#1137,.T.);
#749=FACE_OUTER_BOUND('',#1138,.T.);
#750=FACE_OUTER_BOUND('',#1140,.T.);
#751=FACE_OUTER_BOUND('',#1141,.T.);
#752=FACE_OUTER_BOUND('',#1143,.T.);
#753=FACE_OUTER_BOUND('',#1144,.T.);
#754=FACE_OUTER_BOUND('',#1145,.T.);
#755=FACE_OUTER_BOUND('',#1146,.T.);
#756=FACE_OUTER_BOUND('',#1147,.T.);
#757=FACE_OUTER_BOUND('',#1148,.T.);
#758=FACE_OUTER_BOUND('',#1150,.T.);
#759=FACE_OUTER_BOUND('',#1151,.T.);
#760=FACE_OUTER_BOUND('',#1152,.T.);
#1129=EDGE_LOOP('',(#4074,#4075,#4076,#4077));
#1130=EDGE_LOOP('',(#4078,#4079,#4080));
#1131=EDGE_LOOP('',(#4081));
#1132=EDGE_LOOP('',(#4082,#4083));
#1133=EDGE_LOOP('',(#4084));
#1134=EDGE_LOOP('',(#4085,#4086,#4087,#4088));
#1135=EDGE_LOOP('',(#4089,#4090));
#1136=EDGE_LOOP('',(#4091));
#1137=EDGE_LOOP('',(#4092,#4093,#4094,#4095));
#1138=EDGE_LOOP('',(#4096,#4097));
#1139=EDGE_LOOP('',(#4098));
#1140=EDGE_LOOP('',(#4099,#4100,#4101,#4102));
#1141=EDGE_LOOP('',(#4103,#4104,#4105,#4106,#4107,#4108,#4109,#4110));
#1142=EDGE_LOOP('',(#4111));
#1143=EDGE_LOOP('',(#4112,#4113,#4114,#4115));
#1144=EDGE_LOOP('',(#4116,#4117,#4118,#4119));
#1145=EDGE_LOOP('',(#4120,#4121,#4122,#4123));
#1146=EDGE_LOOP('',(#4124,#4125,#4126,#4127));
#1147=EDGE_LOOP('',(#4128,#4129,#4130,#4131));
#1148=EDGE_LOOP('',(#4132));
#1149=EDGE_LOOP('',(#4133));
#1150=EDGE_LOOP('',(#4134,#4135,#4136,#4137));
#1151=EDGE_LOOP('',(#4138,#4139,#4140,#4141,#4142,#4143,#4144,#4145,#4146,
#4147,#4148,#4149,#4150,#4151,#4152,#4153,#4154,#4155,#4156,#4157));
#1152=EDGE_LOOP('',(#4158));
#1153=EDGE_LOOP('',(#4159));
#1154=EDGE_LOOP('',(#4160));
#1155=EDGE_LOOP('',(#4161));
#1156=EDGE_LOOP('',(#4162));
#1157=EDGE_LOOP('',(#4163));
#1525=LINE('',#8972,#1883);
#1526=LINE('',#8976,#1884);
#1527=LINE('',#8993,#1885);
#1528=LINE('',#8996,#1886);
#1529=LINE('',#9006,#1887);
#1530=LINE('',#9009,#1888);
#1531=LINE('',#9019,#1889);
#1532=LINE('',#9022,#1890);
#1533=LINE('',#9033,#1891);
#1534=LINE('',#9037,#1892);
#1535=LINE('',#9041,#1893);
#1536=LINE('',#9045,#1894);
#1537=LINE('',#9050,#1895);
#1538=LINE('',#9056,#1896);
#1539=LINE('',#9059,#1897);
#1883=VECTOR('',#7133,1.);
#1884=VECTOR('',#7136,1.);
#1885=VECTOR('',#7157,1.);
#1886=VECTOR('',#7160,1.);
#1887=VECTOR('',#7171,1.);
#1888=VECTOR('',#7174,1.);
#1889=VECTOR('',#7185,1.);
#1890=VECTOR('',#7188,1.);
#1891=VECTOR('',#7205,0.225);
#1892=VECTOR('',#7210,0.225);
#1893=VECTOR('',#7215,0.225);
#1894=VECTOR('',#7220,0.225);
#1895=VECTOR('',#7225,1.49);
#1896=VECTOR('',#7234,0.71);
#1897=VECTOR('',#7237,2.);
#2236=CIRCLE('',#6115,0.375);
#2237=CIRCLE('',#6116,0.375);
#2238=CIRCLE('',#6118,2.);
#2239=CIRCLE('',#6119,2.);
#2240=CIRCLE('',#6120,0.225);
#2241=CIRCLE('',#6122,2.);
#2242=CIRCLE('',#6123,0.375);
#2243=CIRCLE('',#6124,0.225);
#2244=CIRCLE('',#6126,0.375);
#2245=CIRCLE('',#6128,2.);
#2246=CIRCLE('',#6129,0.375);
#2247=CIRCLE('',#6130,0.225);
#2248=CIRCLE('',#6132,0.375);
#2249=CIRCLE('',#6134,2.);
#2250=CIRCLE('',#6135,0.375);
#2251=CIRCLE('',#6136,0.225);
#2252=CIRCLE('',#6138,0.375);
#2253=CIRCLE('',#6140,2.);
#2254=CIRCLE('',#6141,2.);
#2255=CIRCLE('',#6142,2.);
#2256=CIRCLE('',#6143,2.);
#2257=CIRCLE('',#6144,0.71);
#2258=CIRCLE('',#6146,0.225);
#2259=CIRCLE('',#6148,0.225);
#2260=CIRCLE('',#6150,0.225);
#2261=CIRCLE('',#6152,0.225);
#2262=CIRCLE('',#6154,1.49);
#2263=CIRCLE('',#6155,1.49);
#2264=CIRCLE('',#6157,0.71);
#2265=CIRCLE('',#6160,2.);
#2604=VERTEX_POINT('',#8970);
#2605=VERTEX_POINT('',#8971);
#2606=VERTEX_POINT('',#8973);
#2607=VERTEX_POINT('',#8975);
#2608=VERTEX_POINT('',#8979);
#2609=VERTEX_POINT('',#8982);
#2610=VERTEX_POINT('',#8985);
#2611=VERTEX_POINT('',#8986);
#2612=VERTEX_POINT('',#8989);
#2613=VERTEX_POINT('',#8992);
#2614=VERTEX_POINT('',#8994);
#2615=VERTEX_POINT('',#8998);
#2616=VERTEX_POINT('',#8999);
#2617=VERTEX_POINT('',#9002);
#2618=VERTEX_POINT('',#9005);
#2619=VERTEX_POINT('',#9007);
#2620=VERTEX_POINT('',#9011);
#2621=VERTEX_POINT('',#9012);
#2622=VERTEX_POINT('',#9015);
#2623=VERTEX_POINT('',#9018);
#2624=VERTEX_POINT('',#9020);
#2625=VERTEX_POINT('',#9028);
#2626=VERTEX_POINT('',#9031);
#2627=VERTEX_POINT('',#9035);
#2628=VERTEX_POINT('',#9039);
#2629=VERTEX_POINT('',#9043);
#2630=VERTEX_POINT('',#9047);
#2631=VERTEX_POINT('',#9049);
#2632=VERTEX_POINT('',#9053);
#2633=VERTEX_POINT('',#9058);
#3159=EDGE_CURVE('',#2604,#2605,#1525,.T.);
#3160=EDGE_CURVE('',#2606,#2604,#2236,.T.);
#3161=EDGE_CURVE('',#2607,#2606,#1526,.T.);
#3162=EDGE_CURVE('',#2605,#2607,#2237,.T.);
#3163=EDGE_CURVE('',#2606,#2608,#2238,.T.);
#3164=EDGE_CURVE('',#2608,#2604,#2239,.T.);
#3165=EDGE_CURVE('',#2609,#2609,#2240,.T.);
#3166=EDGE_CURVE('',#2610,#2611,#2241,.T.);
#3167=EDGE_CURVE('',#2610,#2611,#2242,.T.);
#3168=EDGE_CURVE('',#2612,#2612,#2243,.T.);
#3169=EDGE_CURVE('',#2613,#2610,#1527,.T.);
#3170=EDGE_CURVE('',#2614,#2613,#2244,.T.);
#3171=EDGE_CURVE('',#2611,#2614,#1528,.T.);
#3172=EDGE_CURVE('',#2615,#2616,#2245,.T.);
#3173=EDGE_CURVE('',#2615,#2616,#2246,.T.);
#3174=EDGE_CURVE('',#2617,#2617,#2247,.T.);
#3175=EDGE_CURVE('',#2618,#2615,#1529,.T.);
#3176=EDGE_CURVE('',#2619,#2618,#2248,.T.);
#3177=EDGE_CURVE('',#2616,#2619,#1530,.T.);
#3178=EDGE_CURVE('',#2620,#2621,#2249,.T.);
#3179=EDGE_CURVE('',#2620,#2621,#2250,.T.);
#3180=EDGE_CURVE('',#2622,#2622,#2251,.T.);
#3181=EDGE_CURVE('',#2623,#2620,#1531,.T.);
#3182=EDGE_CURVE('',#2624,#2623,#2252,.T.);
#3183=EDGE_CURVE('',#2621,#2624,#1532,.T.);
#3184=EDGE_CURVE('',#2607,#2624,#2253,.T.);
#3185=EDGE_CURVE('',#2623,#2619,#2254,.T.);
#3186=EDGE_CURVE('',#2618,#2614,#2255,.T.);
#3187=EDGE_CURVE('',#2613,#2605,#2256,.T.);
#3188=EDGE_CURVE('',#2625,#2625,#2257,.T.);
#3189=EDGE_CURVE('',#2626,#2626,#2258,.T.);
#3190=EDGE_CURVE('',#2626,#2609,#1533,.T.);
#3191=EDGE_CURVE('',#2627,#2627,#2259,.T.);
#3192=EDGE_CURVE('',#2627,#2612,#1534,.T.);
#3193=EDGE_CURVE('',#2628,#2628,#2260,.T.);
#3194=EDGE_CURVE('',#2628,#2617,#1535,.T.);
#3195=EDGE_CURVE('',#2629,#2629,#2261,.T.);
#3196=EDGE_CURVE('',#2629,#2622,#1536,.T.);
#3197=EDGE_CURVE('',#2630,#2630,#2262,.T.);
#3198=EDGE_CURVE('',#2630,#2631,#1537,.T.);
#3199=EDGE_CURVE('',#2631,#2631,#2263,.T.);
#3200=EDGE_CURVE('',#2632,#2632,#2264,.T.);
#3201=EDGE_CURVE('',#2625,#2632,#1538,.T.);
#3202=EDGE_CURVE('',#2608,#2633,#1539,.T.);
#3203=EDGE_CURVE('',#2633,#2633,#2265,.T.);
#4074=ORIENTED_EDGE('',*,*,#3159,.F.);
#4075=ORIENTED_EDGE('',*,*,#3160,.F.);
#4076=ORIENTED_EDGE('',*,*,#3161,.F.);
#4077=ORIENTED_EDGE('',*,*,#3162,.F.);
#4078=ORIENTED_EDGE('',*,*,#3163,.F.);
#4079=ORIENTED_EDGE('',*,*,#3160,.T.);
#4080=ORIENTED_EDGE('',*,*,#3164,.F.);
#4081=ORIENTED_EDGE('',*,*,#3165,.F.);
#4082=ORIENTED_EDGE('',*,*,#3166,.F.);
#4083=ORIENTED_EDGE('',*,*,#3167,.T.);
#4084=ORIENTED_EDGE('',*,*,#3168,.F.);
#4085=ORIENTED_EDGE('',*,*,#3169,.F.);
#4086=ORIENTED_EDGE('',*,*,#3170,.F.);
#4087=ORIENTED_EDGE('',*,*,#3171,.F.);
#4088=ORIENTED_EDGE('',*,*,#3167,.F.);
#4089=ORIENTED_EDGE('',*,*,#3172,.F.);
#4090=ORIENTED_EDGE('',*,*,#3173,.T.);
#4091=ORIENTED_EDGE('',*,*,#3174,.F.);
#4092=ORIENTED_EDGE('',*,*,#3175,.F.);
#4093=ORIENTED_EDGE('',*,*,#3176,.F.);
#4094=ORIENTED_EDGE('',*,*,#3177,.F.);
#4095=ORIENTED_EDGE('',*,*,#3173,.F.);
#4096=ORIENTED_EDGE('',*,*,#3178,.F.);
#4097=ORIENTED_EDGE('',*,*,#3179,.T.);
#4098=ORIENTED_EDGE('',*,*,#3180,.F.);
#4099=ORIENTED_EDGE('',*,*,#3181,.F.);
#4100=ORIENTED_EDGE('',*,*,#3182,.F.);
#4101=ORIENTED_EDGE('',*,*,#3183,.F.);
#4102=ORIENTED_EDGE('',*,*,#3179,.F.);
#4103=ORIENTED_EDGE('',*,*,#3162,.T.);
#4104=ORIENTED_EDGE('',*,*,#3184,.T.);
#4105=ORIENTED_EDGE('',*,*,#3182,.T.);
#4106=ORIENTED_EDGE('',*,*,#3185,.T.);
#4107=ORIENTED_EDGE('',*,*,#3176,.T.);
#4108=ORIENTED_EDGE('',*,*,#3186,.T.);
#4109=ORIENTED_EDGE('',*,*,#3170,.T.);
#4110=ORIENTED_EDGE('',*,*,#3187,.T.);
#4111=ORIENTED_EDGE('',*,*,#3188,.T.);
#4112=ORIENTED_EDGE('',*,*,#3189,.F.);
#4113=ORIENTED_EDGE('',*,*,#3190,.T.);
#4114=ORIENTED_EDGE('',*,*,#3165,.T.);
#4115=ORIENTED_EDGE('',*,*,#3190,.F.);
#4116=ORIENTED_EDGE('',*,*,#3191,.F.);
#4117=ORIENTED_EDGE('',*,*,#3192,.T.);
#4118=ORIENTED_EDGE('',*,*,#3168,.T.);
#4119=ORIENTED_EDGE('',*,*,#3192,.F.);
#4120=ORIENTED_EDGE('',*,*,#3193,.F.);
#4121=ORIENTED_EDGE('',*,*,#3194,.T.);
#4122=ORIENTED_EDGE('',*,*,#3174,.T.);
#4123=ORIENTED_EDGE('',*,*,#3194,.F.);
#4124=ORIENTED_EDGE('',*,*,#3195,.F.);
#4125=ORIENTED_EDGE('',*,*,#3196,.T.);
#4126=ORIENTED_EDGE('',*,*,#3180,.T.);
#4127=ORIENTED_EDGE('',*,*,#3196,.F.);
#4128=ORIENTED_EDGE('',*,*,#3197,.F.);
#4129=ORIENTED_EDGE('',*,*,#3198,.T.);
#4130=ORIENTED_EDGE('',*,*,#3199,.T.);
#4131=ORIENTED_EDGE('',*,*,#3198,.F.);
#4132=ORIENTED_EDGE('',*,*,#3199,.F.);
#4133=ORIENTED_EDGE('',*,*,#3200,.F.);
#4134=ORIENTED_EDGE('',*,*,#3188,.F.);
#4135=ORIENTED_EDGE('',*,*,#3201,.T.);
#4136=ORIENTED_EDGE('',*,*,#3200,.T.);
#4137=ORIENTED_EDGE('',*,*,#3201,.F.);
#4138=ORIENTED_EDGE('',*,*,#3159,.T.);
#4139=ORIENTED_EDGE('',*,*,#3187,.F.);
#4140=ORIENTED_EDGE('',*,*,#3169,.T.);
#4141=ORIENTED_EDGE('',*,*,#3166,.T.);
#4142=ORIENTED_EDGE('',*,*,#3171,.T.);
#4143=ORIENTED_EDGE('',*,*,#3186,.F.);
#4144=ORIENTED_EDGE('',*,*,#3175,.T.);
#4145=ORIENTED_EDGE('',*,*,#3172,.T.);
#4146=ORIENTED_EDGE('',*,*,#3177,.T.);
#4147=ORIENTED_EDGE('',*,*,#3185,.F.);
#4148=ORIENTED_EDGE('',*,*,#3181,.T.);
#4149=ORIENTED_EDGE('',*,*,#3178,.T.);
#4150=ORIENTED_EDGE('',*,*,#3183,.T.);
#4151=ORIENTED_EDGE('',*,*,#3184,.F.);
#4152=ORIENTED_EDGE('',*,*,#3161,.T.);
#4153=ORIENTED_EDGE('',*,*,#3163,.T.);
#4154=ORIENTED_EDGE('',*,*,#3202,.T.);
#4155=ORIENTED_EDGE('',*,*,#3203,.T.);
#4156=ORIENTED_EDGE('',*,*,#3202,.F.);
#4157=ORIENTED_EDGE('',*,*,#3164,.T.);
#4158=ORIENTED_EDGE('',*,*,#3203,.F.);
#4159=ORIENTED_EDGE('',*,*,#3197,.T.);
#4160=ORIENTED_EDGE('',*,*,#3195,.T.);
#4161=ORIENTED_EDGE('',*,*,#3193,.T.);
#4162=ORIENTED_EDGE('',*,*,#3191,.T.);
#4163=ORIENTED_EDGE('',*,*,#3189,.T.);
#5213=CYLINDRICAL_SURFACE('',#6114,0.375);
#5214=CYLINDRICAL_SURFACE('',#6125,0.375);
#5215=CYLINDRICAL_SURFACE('',#6131,0.375);
#5216=CYLINDRICAL_SURFACE('',#6137,0.375);
#5217=CYLINDRICAL_SURFACE('',#6145,0.225);
#5218=CYLINDRICAL_SURFACE('',#6147,0.225);
#5219=CYLINDRICAL_SURFACE('',#6149,0.225);
#5220=CYLINDRICAL_SURFACE('',#6151,0.225);
#5221=CYLINDRICAL_SURFACE('',#6153,1.49);
#5222=CYLINDRICAL_SURFACE('',#6158,0.71);
#5223=CYLINDRICAL_SURFACE('',#6159,2.);
#5386=ADVANCED_FACE('',(#743),#5213,.F.);
#5387=ADVANCED_FACE('',(#744,#411),#521,.T.);
#5388=ADVANCED_FACE('',(#745,#412),#522,.T.);
#5389=ADVANCED_FACE('',(#746),#5214,.F.);
#5390=ADVANCED_FACE('',(#747,#413),#523,.T.);
#5391=ADVANCED_FACE('',(#748),#5215,.F.);
#5392=ADVANCED_FACE('',(#749,#414),#524,.T.);
#5393=ADVANCED_FACE('',(#750),#5216,.F.);
#5394=ADVANCED_FACE('',(#751,#415),#525,.T.);
#5395=ADVANCED_FACE('',(#752),#5217,.F.);
#5396=ADVANCED_FACE('',(#753),#5218,.F.);
#5397=ADVANCED_FACE('',(#754),#5219,.F.);
#5398=ADVANCED_FACE('',(#755),#5220,.F.);
#5399=ADVANCED_FACE('',(#756),#5221,.T.);
#5400=ADVANCED_FACE('',(#757,#416),#526,.F.);
#5401=ADVANCED_FACE('',(#758),#5222,.F.);
#5402=ADVANCED_FACE('',(#759),#5223,.T.);
#5403=ADVANCED_FACE('',(#760,#417,#418,#419,#420,#421),#527,.F.);
#5633=CLOSED_SHELL('',(#5386,#5387,#5388,#5389,#5390,#5391,#5392,#5393,
#5394,#5395,#5396,#5397,#5398,#5399,#5400,#5401,#5402,#5403));
#6113=AXIS2_PLACEMENT_3D('',#8968,#7129,#7130);
#6114=AXIS2_PLACEMENT_3D('',#8969,#7131,#7132);
#6115=AXIS2_PLACEMENT_3D('',#8974,#7134,#7135);
#6116=AXIS2_PLACEMENT_3D('',#8977,#7137,#7138);
#6117=AXIS2_PLACEMENT_3D('',#8978,#7139,#7140);
#6118=AXIS2_PLACEMENT_3D('',#8980,#7141,#7142);
#6119=AXIS2_PLACEMENT_3D('',#8981,#7143,#7144);
#6120=AXIS2_PLACEMENT_3D('',#8983,#7145,#7146);
#6121=AXIS2_PLACEMENT_3D('',#8984,#7147,#7148);
#6122=AXIS2_PLACEMENT_3D('',#8987,#7149,#7150);
#6123=AXIS2_PLACEMENT_3D('',#8988,#7151,#7152);
#6124=AXIS2_PLACEMENT_3D('',#8990,#7153,#7154);
#6125=AXIS2_PLACEMENT_3D('',#8991,#7155,#7156);
#6126=AXIS2_PLACEMENT_3D('',#8995,#7158,#7159);
#6127=AXIS2_PLACEMENT_3D('',#8997,#7161,#7162);
#6128=AXIS2_PLACEMENT_3D('',#9000,#7163,#7164);
#6129=AXIS2_PLACEMENT_3D('',#9001,#7165,#7166);
#6130=AXIS2_PLACEMENT_3D('',#9003,#7167,#7168);
#6131=AXIS2_PLACEMENT_3D('',#9004,#7169,#7170);
#6132=AXIS2_PLACEMENT_3D('',#9008,#7172,#7173);
#6133=AXIS2_PLACEMENT_3D('',#9010,#7175,#7176);
#6134=AXIS2_PLACEMENT_3D('',#9013,#7177,#7178);
#6135=AXIS2_PLACEMENT_3D('',#9014,#7179,#7180);
#6136=AXIS2_PLACEMENT_3D('',#9016,#7181,#7182);
#6137=AXIS2_PLACEMENT_3D('',#9017,#7183,#7184);
#6138=AXIS2_PLACEMENT_3D('',#9021,#7186,#7187);
#6139=AXIS2_PLACEMENT_3D('',#9023,#7189,#7190);
#6140=AXIS2_PLACEMENT_3D('',#9024,#7191,#7192);
#6141=AXIS2_PLACEMENT_3D('',#9025,#7193,#7194);
#6142=AXIS2_PLACEMENT_3D('',#9026,#7195,#7196);
#6143=AXIS2_PLACEMENT_3D('',#9027,#7197,#7198);
#6144=AXIS2_PLACEMENT_3D('',#9029,#7199,#7200);
#6145=AXIS2_PLACEMENT_3D('',#9030,#7201,#7202);
#6146=AXIS2_PLACEMENT_3D('',#9032,#7203,#7204);
#6147=AXIS2_PLACEMENT_3D('',#9034,#7206,#7207);
#6148=AXIS2_PLACEMENT_3D('',#9036,#7208,#7209);
#6149=AXIS2_PLACEMENT_3D('',#9038,#7211,#7212);
#6150=AXIS2_PLACEMENT_3D('',#9040,#7213,#7214);
#6151=AXIS2_PLACEMENT_3D('',#9042,#7216,#7217);
#6152=AXIS2_PLACEMENT_3D('',#9044,#7218,#7219);
#6153=AXIS2_PLACEMENT_3D('',#9046,#7221,#7222);
#6154=AXIS2_PLACEMENT_3D('',#9048,#7223,#7224);
#6155=AXIS2_PLACEMENT_3D('',#9051,#7226,#7227);
#6156=AXIS2_PLACEMENT_3D('',#9052,#7228,#7229);
#6157=AXIS2_PLACEMENT_3D('',#9054,#7230,#7231);
#6158=AXIS2_PLACEMENT_3D('',#9055,#7232,#7233);
#6159=AXIS2_PLACEMENT_3D('',#9057,#7235,#7236);
#6160=AXIS2_PLACEMENT_3D('',#9060,#7238,#7239);
#6161=AXIS2_PLACEMENT_3D('',#9061,#7240,#7241);
#7129=DIRECTION('axis',(0.,0.,1.));
#7130=DIRECTION('refdir',(1.,0.,0.));
#7131=DIRECTION('center_axis',(0.,0.,1.));
#7132=DIRECTION('ref_axis',(1.,0.,0.));
#7133=DIRECTION('',(0.,0.,1.));
#7134=DIRECTION('center_axis',(0.,0.,1.));
#7135=DIRECTION('ref_axis',(1.,0.,0.));
#7136=DIRECTION('',(0.,0.,-1.));
#7137=DIRECTION('center_axis',(0.,0.,-1.));
#7138=DIRECTION('ref_axis',(1.,0.,0.));
#7139=DIRECTION('center_axis',(0.,0.,1.));
#7140=DIRECTION('ref_axis',(1.,0.,0.));
#7141=DIRECTION('center_axis',(0.,0.,-1.));
#7142=DIRECTION('ref_axis',(1.,0.,0.));
#7143=DIRECTION('center_axis',(0.,0.,-1.));
#7144=DIRECTION('ref_axis',(1.,0.,0.));
#7145=DIRECTION('center_axis',(0.,0.,1.));
#7146=DIRECTION('ref_axis',(1.,0.,0.));
#7147=DIRECTION('center_axis',(0.,0.,1.));
#7148=DIRECTION('ref_axis',(1.,0.,0.));
#7149=DIRECTION('center_axis',(0.,0.,-1.));
#7150=DIRECTION('ref_axis',(1.,0.,0.));
#7151=DIRECTION('center_axis',(0.,0.,1.));
#7152=DIRECTION('ref_axis',(1.,0.,0.));
#7153=DIRECTION('center_axis',(0.,0.,1.));
#7154=DIRECTION('ref_axis',(1.,0.,0.));
#7155=DIRECTION('center_axis',(0.,0.,1.));
#7156=DIRECTION('ref_axis',(-1.83697019872103E-16,-1.,0.));
#7157=DIRECTION('',(0.,0.,-1.));
#7158=DIRECTION('center_axis',(0.,0.,-1.));
#7159=DIRECTION('ref_axis',(1.,0.,0.));
#7160=DIRECTION('',(0.,0.,1.));
#7161=DIRECTION('center_axis',(0.,0.,1.));
#7162=DIRECTION('ref_axis',(1.,0.,0.));
#7163=DIRECTION('center_axis',(0.,0.,-1.));
#7164=DIRECTION('ref_axis',(1.,0.,0.));
#7165=DIRECTION('center_axis',(0.,0.,1.));
#7166=DIRECTION('ref_axis',(1.,0.,0.));
#7167=DIRECTION('center_axis',(0.,0.,1.));
#7168=DIRECTION('ref_axis',(1.,0.,0.));
#7169=DIRECTION('center_axis',(0.,0.,1.));
#7170=DIRECTION('ref_axis',(-1.,1.22464679914735E-16,0.));
#7171=DIRECTION('',(0.,0.,-1.));
#7172=DIRECTION('center_axis',(0.,0.,-1.));
#7173=DIRECTION('ref_axis',(1.,0.,0.));
#7174=DIRECTION('',(0.,0.,1.));
#7175=DIRECTION('center_axis',(0.,0.,1.));
#7176=DIRECTION('ref_axis',(1.,0.,0.));
#7177=DIRECTION('center_axis',(0.,0.,-1.));
#7178=DIRECTION('ref_axis',(1.,0.,0.));
#7179=DIRECTION('center_axis',(0.,0.,1.));
#7180=DIRECTION('ref_axis',(1.,0.,0.));
#7181=DIRECTION('center_axis',(0.,0.,1.));
#7182=DIRECTION('ref_axis',(1.,0.,0.));
#7183=DIRECTION('center_axis',(0.,0.,1.));
#7184=DIRECTION('ref_axis',(-6.04901474817726E-16,1.,0.));
#7185=DIRECTION('',(0.,0.,-1.));
#7186=DIRECTION('center_axis',(0.,0.,-1.));
#7187=DIRECTION('ref_axis',(1.,0.,0.));
#7188=DIRECTION('',(0.,0.,1.));
#7189=DIRECTION('center_axis',(0.,0.,1.));
#7190=DIRECTION('ref_axis',(1.,0.,0.));
#7191=DIRECTION('center_axis',(0.,0.,1.));
#7192=DIRECTION('ref_axis',(1.,0.,0.));
#7193=DIRECTION('center_axis',(0.,0.,1.));
#7194=DIRECTION('ref_axis',(1.,0.,0.));
#7195=DIRECTION('center_axis',(0.,0.,1.));
#7196=DIRECTION('ref_axis',(1.,0.,0.));
#7197=DIRECTION('center_axis',(0.,0.,1.));
#7198=DIRECTION('ref_axis',(1.,0.,0.));
#7199=DIRECTION('center_axis',(0.,0.,-1.));
#7200=DIRECTION('ref_axis',(1.,0.,0.));
#7201=DIRECTION('center_axis',(0.,0.,1.));
#7202=DIRECTION('ref_axis',(1.,0.,0.));
#7203=DIRECTION('center_axis',(0.,0.,1.));
#7204=DIRECTION('ref_axis',(1.,0.,0.));
#7205=DIRECTION('',(0.,0.,1.));
#7206=DIRECTION('center_axis',(0.,0.,1.));
#7207=DIRECTION('ref_axis',(1.,0.,0.));
#7208=DIRECTION('center_axis',(0.,0.,1.));
#7209=DIRECTION('ref_axis',(1.,0.,0.));
#7210=DIRECTION('',(0.,0.,1.));
#7211=DIRECTION('center_axis',(0.,0.,1.));
#7212=DIRECTION('ref_axis',(1.,0.,0.));
#7213=DIRECTION('center_axis',(0.,0.,1.));
#7214=DIRECTION('ref_axis',(1.,0.,0.));
#7215=DIRECTION('',(0.,0.,1.));
#7216=DIRECTION('center_axis',(0.,0.,1.));
#7217=DIRECTION('ref_axis',(1.,0.,0.));
#7218=DIRECTION('center_axis',(0.,0.,1.));
#7219=DIRECTION('ref_axis',(1.,0.,0.));
#7220=DIRECTION('',(0.,0.,1.));
#7221=DIRECTION('center_axis',(0.,0.,1.));
#7222=DIRECTION('ref_axis',(1.,0.,0.));
#7223=DIRECTION('center_axis',(0.,0.,1.));
#7224=DIRECTION('ref_axis',(1.,0.,0.));
#7225=DIRECTION('',(0.,0.,-1.));
#7226=DIRECTION('center_axis',(0.,0.,1.));
#7227=DIRECTION('ref_axis',(1.,0.,0.));
#7228=DIRECTION('center_axis',(0.,0.,1.));
#7229=DIRECTION('ref_axis',(1.,0.,0.));
#7230=DIRECTION('center_axis',(0.,0.,-1.));
#7231=DIRECTION('ref_axis',(1.,0.,0.));
#7232=DIRECTION('center_axis',(0.,0.,1.));
#7233=DIRECTION('ref_axis',(1.,0.,0.));
#7234=DIRECTION('',(0.,0.,-1.));
#7235=DIRECTION('center_axis',(0.,0.,1.));
#7236=DIRECTION('ref_axis',(1.,0.,0.));
#7237=DIRECTION('',(0.,0.,-1.));
#7238=DIRECTION('center_axis',(0.,0.,1.));
#7239=DIRECTION('ref_axis',(1.,0.,0.));
#7240=DIRECTION('center_axis',(0.,0.,1.));
#7241=DIRECTION('ref_axis',(1.,0.,0.));
#8968=CARTESIAN_POINT('',(0.,0.,0.));
#8969=CARTESIAN_POINT('Origin',(2.52264068711929,2.10639249453345E-16,4.));
#8970=CARTESIAN_POINT('',(2.26072934990998,0.268379305165721,4.));
#8971=CARTESIAN_POINT('',(2.26072934990998,0.268379305165722,4.4));
#8972=CARTESIAN_POINT('',(2.26072934990998,0.268379305165721,4.));
#8973=CARTESIAN_POINT('',(2.26072934990998,-0.268379305165721,4.));
#8974=CARTESIAN_POINT('Origin',(2.52264068711929,2.10639249453345E-16,4.));
#8975=CARTESIAN_POINT('',(2.26072934990998,-0.268379305165721,4.4));
#8976=CARTESIAN_POINT('',(2.26072934990998,-0.268379305165721,4.));
#8977=CARTESIAN_POINT('Origin',(2.52264068711929,2.10639249453345E-16,4.4));
#8978=CARTESIAN_POINT('Origin',(2.52264068711929,2.22044604925031E-16,4.));
#8979=CARTESIAN_POINT('',(2.24264068711929,-2.44929359829471E-16,4.));
#8980=CARTESIAN_POINT('Origin',(4.24264068711929,0.,4.));
#8981=CARTESIAN_POINT('Origin',(4.24264068711929,0.,4.));
#8982=CARTESIAN_POINT('',(2.29764068711929,1.83084696472529E-16,4.));
#8983=CARTESIAN_POINT('Origin',(2.52264068711929,2.10639249453345E-16,4.));
#8984=CARTESIAN_POINT('Origin',(4.24264068711929,1.72,4.));
#8985=CARTESIAN_POINT('',(3.97426138195357,1.9819113372093,4.));
#8986=CARTESIAN_POINT('',(4.51101999228501,1.9819113372093,4.));
#8987=CARTESIAN_POINT('Origin',(4.24264068711929,0.,4.));
#8988=CARTESIAN_POINT('Origin',(4.24264068711929,1.72,4.));
#8989=CARTESIAN_POINT('',(4.01764068711929,1.72,4.));
#8990=CARTESIAN_POINT('Origin',(4.24264068711929,1.72,4.));
#8991=CARTESIAN_POINT('Origin',(4.24264068711929,1.72,4.));
#8992=CARTESIAN_POINT('',(3.97426138195357,1.9819113372093,4.4));
#8993=CARTESIAN_POINT('',(3.97426138195357,1.9819113372093,4.));
#8994=CARTESIAN_POINT('',(4.51101999228501,1.9819113372093,4.4));
#8995=CARTESIAN_POINT('Origin',(4.24264068711929,1.72,4.4));
#8996=CARTESIAN_POINT('',(4.51101999228501,1.9819113372093,4.));
#8997=CARTESIAN_POINT('Origin',(5.96264068711929,0.,4.));
#8998=CARTESIAN_POINT('',(6.22455202432859,0.268379305165721,4.));
#8999=CARTESIAN_POINT('',(6.22455202432859,-0.268379305165721,4.));
#9000=CARTESIAN_POINT('Origin',(4.24264068711929,0.,4.));
#9001=CARTESIAN_POINT('Origin',(5.96264068711929,0.,4.));
#9002=CARTESIAN_POINT('',(5.73764068711929,-2.75545529808154E-17,4.));
#9003=CARTESIAN_POINT('Origin',(5.96264068711929,0.,4.));
#9004=CARTESIAN_POINT('Origin',(5.96264068711929,0.,4.));
#9005=CARTESIAN_POINT('',(6.22455202432859,0.26837930516572,4.4));
#9006=CARTESIAN_POINT('',(6.22455202432859,0.268379305165721,4.));
#9007=CARTESIAN_POINT('',(6.22455202432859,-0.26837930516572,4.4));
#9008=CARTESIAN_POINT('Origin',(5.96264068711929,0.,4.4));
#9009=CARTESIAN_POINT('',(6.22455202432859,-0.268379305165721,4.));
#9010=CARTESIAN_POINT('Origin',(4.24264068711929,-1.72,4.));
#9011=CARTESIAN_POINT('',(4.51101999228501,-1.9819113372093,4.));
#9012=CARTESIAN_POINT('',(3.97426138195357,-1.9819113372093,4.));
#9013=CARTESIAN_POINT('Origin',(4.24264068711929,0.,4.));
#9014=CARTESIAN_POINT('Origin',(4.24264068711929,-1.72,4.));
#9015=CARTESIAN_POINT('',(4.01764068711929,-1.72,4.));
#9016=CARTESIAN_POINT('Origin',(4.24264068711929,-1.72,4.));
#9017=CARTESIAN_POINT('Origin',(4.24264068711929,-1.72,4.));
#9018=CARTESIAN_POINT('',(4.51101999228501,-1.9819113372093,4.4));
#9019=CARTESIAN_POINT('',(4.51101999228501,-1.9819113372093,4.));
#9020=CARTESIAN_POINT('',(3.97426138195357,-1.9819113372093,4.4));
#9021=CARTESIAN_POINT('Origin',(4.24264068711929,-1.72,4.4));
#9022=CARTESIAN_POINT('',(3.97426138195357,-1.9819113372093,4.));
#9023=CARTESIAN_POINT('Origin',(4.24264068711929,0.,4.4));
#9024=CARTESIAN_POINT('Origin',(4.24264068711929,0.,4.4));
#9025=CARTESIAN_POINT('Origin',(4.24264068711929,0.,4.4));
#9026=CARTESIAN_POINT('Origin',(4.24264068711929,0.,4.4));
#9027=CARTESIAN_POINT('Origin',(4.24264068711929,0.,4.4));
#9028=CARTESIAN_POINT('',(3.53264068711929,-8.69499227394621E-17,4.4));
#9029=CARTESIAN_POINT('Origin',(4.24264068711929,0.,4.4));
#9030=CARTESIAN_POINT('Origin',(2.52264068711929,2.10639249453345E-16,3.5));
#9031=CARTESIAN_POINT('',(2.29764068711929,1.83084696472529E-16,3.6));
#9032=CARTESIAN_POINT('Origin',(2.52264068711929,2.10639249453345E-16,3.6));
#9033=CARTESIAN_POINT('',(2.29764068711929,1.83084696472529E-16,3.5));
#9034=CARTESIAN_POINT('Origin',(4.24264068711929,1.72,3.5));
#9035=CARTESIAN_POINT('',(4.01764068711929,1.72,3.6));
#9036=CARTESIAN_POINT('Origin',(4.24264068711929,1.72,3.6));
#9037=CARTESIAN_POINT('',(4.01764068711929,1.72,3.5));
#9038=CARTESIAN_POINT('Origin',(5.96264068711929,0.,3.5));
#9039=CARTESIAN_POINT('',(5.73764068711929,-2.75545529808154E-17,3.6));
#9040=CARTESIAN_POINT('Origin',(5.96264068711929,0.,3.6));
#9041=CARTESIAN_POINT('',(5.73764068711929,-2.75545529808154E-17,3.5));
#9042=CARTESIAN_POINT('Origin',(4.24264068711929,-1.72,3.5));
#9043=CARTESIAN_POINT('',(4.01764068711929,-1.72,3.6));
#9044=CARTESIAN_POINT('Origin',(4.24264068711929,-1.72,3.6));
#9045=CARTESIAN_POINT('',(4.01764068711929,-1.72,3.5));
#9046=CARTESIAN_POINT('Origin',(4.24264068711929,0.,2.95));
#9047=CARTESIAN_POINT('',(2.75264068711929,-1.82472373072956E-16,3.6));
#9048=CARTESIAN_POINT('Origin',(4.24264068711929,0.,3.6));
#9049=CARTESIAN_POINT('',(2.75264068711929,-1.82472373072956E-16,2.95));
#9050=CARTESIAN_POINT('',(2.75264068711929,-1.82472373072956E-16,2.95));
#9051=CARTESIAN_POINT('Origin',(4.24264068711929,0.,2.95));
#9052=CARTESIAN_POINT('Origin',(4.24264068711929,0.,2.95));
#9053=CARTESIAN_POINT('',(3.53264068711929,-8.69499227394621E-17,2.95));
#9054=CARTESIAN_POINT('Origin',(4.24264068711929,0.,2.95));
#9055=CARTESIAN_POINT('Origin',(4.24264068711929,0.,3.6));
#9056=CARTESIAN_POINT('',(3.53264068711929,-8.69499227394621E-17,3.6));
#9057=CARTESIAN_POINT('Origin',(4.24264068711929,0.,3.6));
#9058=CARTESIAN_POINT('',(2.24264068711929,-2.44929359829471E-16,3.6));
#9059=CARTESIAN_POINT('',(2.24264068711929,-2.44929359829471E-16,3.6));
#9060=CARTESIAN_POINT('Origin',(4.24264068711929,0.,3.6));
#9061=CARTESIAN_POINT('Origin',(4.24264068711929,0.,3.6));
#10784=UNCERTAINTY_MEASURE_WITH_UNIT(LENGTH_MEASURE(0.001),#10838,
'DISTANCE_ACCURACY_VALUE',
'Maximum model space distance between geometric entities at asserted c
onnectivities');
#10807=UNCERTAINTY_MEASURE_WITH_UNIT(LENGTH_MEASURE(0.001),#10838,
'DISTANCE_ACCURACY_VALUE',
'Maximum model space distance between geometric entities at asserted c
onnectivities');
#10814=(
GEOMETRIC_REPRESENTATION_CONTEXT(3)
GLOBAL_UNCERTAINTY_ASSIGNED_CONTEXT((#10784))
GLOBAL_UNIT_ASSIGNED_CONTEXT((#10838,#10840,#10841))
REPRESENTATION_CONTEXT('','3D')
);
#10837=(
GEOMETRIC_REPRESENTATION_CONTEXT(3)
GLOBAL_UNCERTAINTY_ASSIGNED_CONTEXT((#10807))
GLOBAL_UNIT_ASSIGNED_CONTEXT((#10838,#10840,#10841))
REPRESENTATION_CONTEXT('','3D')
);
#10838=(
LENGTH_UNIT()
NAMED_UNIT(*)
SI_UNIT(.CENTI.,.METRE.)
);
#10840=(
NAMED_UNIT(*)
PLANE_ANGLE_UNIT()
SI_UNIT($,.RADIAN.)
);
#10841=(
NAMED_UNIT(*)
SI_UNIT($,.STERADIAN.)
SOLID_ANGLE_UNIT()
);
#10848=SHAPE_DEFINITION_REPRESENTATION(#10877,#10947);
#10877=PRODUCT_DEFINITION_SHAPE('',$,#10977);
#10947=SHAPE_REPRESENTATION('',(#6113),#10814);
#10970=PRODUCT_DEFINITION_CONTEXT('part definition',#11059,'design');
#10977=PRODUCT_DEFINITION('Bearing cap (1)','Bearing cap (1)',#11006,#10970);
#11006=PRODUCT_DEFINITION_FORMATION('',$,#11067);
#11059=APPLICATION_CONTEXT(
'Core Data for Automotive Mechanical Design Process');
#11060=PRODUCT_CONTEXT('part definition',#11059,'mechanical');
#11067=PRODUCT('Bearing cap (1)','Bearing cap (1)','Bearing cap (1)',(#11060));
#11160=COLOUR_RGB('Grey',0.48,0.52,0.57);
#11161=FILL_AREA_STYLE_COLOUR('',#11160);
#11162=FILL_AREA_STYLE('',(#11161));
#11163=SURFACE_STYLE_FILL_AREA(#11162);
#11164=SURFACE_SIDE_STYLE('',(#11163));
#11165=SURFACE_STYLE_USAGE(.BOTH.,#11164);
#11166=PRESENTATION_STYLE_ASSIGNMENT((#11165));
ENDSEC;
END-ISO-10303-21;
